ISO-10303-21;
HEADER;
FILE_DESCRIPTION((''),'2;1');
FILE_NAME('Spring_Washer_2.step','2026-10-09T11:34:15-07:00',(''),(''),'','','');
FILE_SCHEMA (('AUTOMOTIVE_DESIGN { 1 0 10303 214 3 1 1 }'));
ENDSEC;
DATA;
#10=MECHANICAL_DESIGN_GEOMETRIC_PRESENTATION_REPRESENTATION('',(#635),#117170);
#593=SHAPE_REPRESENTATION_RELATIONSHIP('SRR','None',#117248,#614) ;
#614=ADVANCED_BREP_SHAPE_REPRESENTATION('',(#656),#117156) ;
#635=STYLED_ITEM('',(#117355),#656) ;
#656=MANIFOLD_SOLID_BREP('Body1',#49064) ;
#730=FACE_BOUND('',#15263,.T.) ;
#2483=PLANE('',#52004) ;
#4267=LINE('',#87505,#7481) ;
#4268=LINE('',#87510,#7482) ;
#7481=VECTOR('',#61714,2.49999999999999) ;
#7482=VECTOR('',#61721,2.69999999999999) ;
#9989=CYLINDRICAL_SURFACE('',#52000,2.49999999999999) ;
#9990=CYLINDRICAL_SURFACE('',#52002,2.69999999999999) ;
#12107=FACE_OUTER_BOUND('',#15259,.T.) ;
#12108=FACE_OUTER_BOUND('',#15260,.T.) ;
#12109=FACE_OUTER_BOUND('',#15261,.T.) ;
#12110=FACE_OUTER_BOUND('',#15262,.T.) ;
#15259=EDGE_LOOP('',(#37292,#37293,#37294,#37295,#37296,#37297)) ;
#15260=EDGE_LOOP('',(#37298,#37299,#37300,#37301,#37302)) ;
#15261=EDGE_LOOP('',(#37303,#37304,#37305,#37306,#37307)) ;
#15262=EDGE_LOOP('',(#37308)) ;
#15263=EDGE_LOOP('',(#37309)) ;
#18393=CIRCLE('',#51995,2.49999999999999) ;
#18394=CIRCLE('',#51996,0.45) ;
#18395=CIRCLE('',#51997,2.69999999999999) ;
#18396=CIRCLE('',#51998,2.69999999999999) ;
#18397=CIRCLE('',#51999,2.49999999999999) ;
#18398=CIRCLE('',#52001,2.49999999999999) ;
#18399=CIRCLE('',#52003,2.69999999999999) ;
#21382=VERTEX_POINT('',#87494) ;
#21383=VERTEX_POINT('',#87495) ;
#21384=VERTEX_POINT('',#87497) ;
#21385=VERTEX_POINT('',#87499) ;
#21386=VERTEX_POINT('',#87504) ;
#21387=VERTEX_POINT('',#87508) ;
#26924=EDGE_CURVE('',#21382,#21383,#18393,.T.) ;
#26925=EDGE_CURVE('',#21383,#21384,#18394,.T.) ;
#26926=EDGE_CURVE('',#21385,#21384,#18395,.T.) ;
#26927=EDGE_CURVE('',#21384,#21385,#18396,.T.) ;
#26928=EDGE_CURVE('',#21383,#21382,#18397,.T.) ;
#26929=EDGE_CURVE('',#21382,#21386,#4267,.T.) ;
#26930=EDGE_CURVE('',#21386,#21386,#18398,.T.) ;
#26931=EDGE_CURVE('',#21387,#21387,#18399,.T.) ;
#26932=EDGE_CURVE('',#21387,#21385,#4268,.T.) ;
#37292=ORIENTED_EDGE('',*,*,#26924,.T.) ;
#37293=ORIENTED_EDGE('',*,*,#26925,.T.) ;
#37294=ORIENTED_EDGE('',*,*,#26926,.F.) ;
#37295=ORIENTED_EDGE('',*,*,#26927,.F.) ;
#37296=ORIENTED_EDGE('',*,*,#26925,.F.) ;
#37297=ORIENTED_EDGE('',*,*,#26928,.T.) ;
#37298=ORIENTED_EDGE('',*,*,#26924,.F.) ;
#37299=ORIENTED_EDGE('',*,*,#26929,.T.) ;
#37300=ORIENTED_EDGE('',*,*,#26930,.F.) ;
#37301=ORIENTED_EDGE('',*,*,#26929,.F.) ;
#37302=ORIENTED_EDGE('',*,*,#26928,.F.) ;
#37303=ORIENTED_EDGE('',*,*,#26931,.F.) ;
#37304=ORIENTED_EDGE('',*,*,#26932,.T.) ;
#37305=ORIENTED_EDGE('',*,*,#26926,.T.) ;
#37306=ORIENTED_EDGE('',*,*,#26927,.T.) ;
#37307=ORIENTED_EDGE('',*,*,#26932,.F.) ;
#37308=ORIENTED_EDGE('',*,*,#26931,.T.) ;
#37309=ORIENTED_EDGE('',*,*,#26930,.T.) ;
#45695=TOROIDAL_SURFACE('',#51994,2.94999999999999,0.45) ;
#47325=ADVANCED_FACE('',(#12107),#45695,.T.) ;
#47326=ADVANCED_FACE('',(#12108),#9989,.F.) ;
#47327=ADVANCED_FACE('',(#12109),#9990,.T.) ;
#47328=ADVANCED_FACE('',(#12110,#730),#2483,.T.) ;
#49064=CLOSED_SHELL('',(#47325,#47326,#47327,#47328)) ;
#51993=AXIS2_PLACEMENT_3D('',#87492,#61698,#61699) ;
#51994=AXIS2_PLACEMENT_3D('',#87493,#61700,#61701) ;
#51995=AXIS2_PLACEMENT_3D('',#87496,#61702,#61703) ;
#51996=AXIS2_PLACEMENT_3D('',#87498,#61704,#61705) ;
#51997=AXIS2_PLACEMENT_3D('',#87500,#61706,#61707) ;
#51998=AXIS2_PLACEMENT_3D('',#87501,#61708,#61709) ;
#51999=AXIS2_PLACEMENT_3D('',#87502,#61710,#61711) ;
#52000=AXIS2_PLACEMENT_3D('',#87503,#61712,#61713) ;
#52001=AXIS2_PLACEMENT_3D('',#87506,#61715,#61716) ;
#52002=AXIS2_PLACEMENT_3D('',#87507,#61717,#61718) ;
#52003=AXIS2_PLACEMENT_3D('',#87509,#61719,#61720) ;
#52004=AXIS2_PLACEMENT_3D('',#87511,#61722,#61723) ;
#61698=DIRECTION('axis',(0.,0.,1.)) ;
#61699=DIRECTION('refdir',(1.,0.,0.)) ;
#61700=DIRECTION('center_axis',(0.,-5.60383084497445E-34,1.)) ;
#61701=DIRECTION('ref_axis',(-1.,0.,0.)) ;
#61702=DIRECTION('center_axis',(0.,5.60383084497445E-34,-1.)) ;
#61703=DIRECTION('ref_axis',(-1.,0.,0.)) ;
#61704=DIRECTION('center_axis',(0.,1.,5.60383084497445E-34)) ;
#61705=DIRECTION('ref_axis',(1.,0.,0.)) ;
#61706=DIRECTION('center_axis',(2.52374105052742E-18,5.60383084497445E-34,
-1.)) ;
#61707=DIRECTION('ref_axis',(1.,3.40207761657885E-68,2.52374105052742E-18)) ;
#61708=DIRECTION('center_axis',(2.52374105052742E-18,5.60383084497445E-34,
-1.)) ;
#61709=DIRECTION('ref_axis',(1.,3.40207761657885E-68,2.52374105052742E-18)) ;
#61710=DIRECTION('center_axis',(0.,5.60383084497445E-34,-1.)) ;
#61711=DIRECTION('ref_axis',(-1.,0.,0.)) ;
#61712=DIRECTION('center_axis',(0.,0.,-1.)) ;
#61713=DIRECTION('ref_axis',(1.,0.,0.)) ;
#61714=DIRECTION('',(0.,0.,-1.)) ;
#61715=DIRECTION('center_axis',(-2.52374105052742E-18,-5.60383084497445E-34,
1.)) ;
#61716=DIRECTION('ref_axis',(1.,3.40207761657885E-68,2.52374105052742E-18)) ;
#61717=DIRECTION('center_axis',(0.,0.,-1.)) ;
#61718=DIRECTION('ref_axis',(1.,0.,0.)) ;
#61719=DIRECTION('center_axis',(2.52374105052742E-18,5.60383084497445E-34,
-1.)) ;
#61720=DIRECTION('ref_axis',(1.,3.40207761657885E-68,2.52374105052742E-18)) ;
#61721=DIRECTION('',(0.,0.,1.)) ;
#61722=DIRECTION('center_axis',(2.52374105052742E-18,5.60383084497445E-34,
-1.)) ;
#61723=DIRECTION('ref_axis',(1.,3.40207761657885E-68,2.52374105052742E-18)) ;
#87492=CARTESIAN_POINT('',(0.,0.,0.)) ;
#87493=CARTESIAN_POINT('Origin',(61.5,261.2,30.3471546048822)) ;
#87494=CARTESIAN_POINT('',(59.,261.2,30.3471546048822)) ;
#87495=CARTESIAN_POINT('',(64.,261.2,30.3471546048822)) ;
#87496=CARTESIAN_POINT('Origin',(61.5,261.2,30.3471546048822)) ;
#87497=CARTESIAN_POINT('',(64.2,261.2,30.7213203435596)) ;
#87498=CARTESIAN_POINT('Origin',(64.45,261.2,30.3471546048822)) ;
#87499=CARTESIAN_POINT('',(58.8,261.2,30.7213203435596)) ;
#87500=CARTESIAN_POINT('Origin',(61.5,261.2,30.7213203435596)) ;
#87501=CARTESIAN_POINT('Origin',(61.5,261.2,30.7213203435596)) ;
#87502=CARTESIAN_POINT('Origin',(61.5,261.2,30.3471546048822)) ;
#87503=CARTESIAN_POINT('Origin',(61.5,261.2,30.7213203435596)) ;
#87504=CARTESIAN_POINT('',(59.,261.2,28.7213203435596)) ;
#87505=CARTESIAN_POINT('',(59.,261.2,30.7213203435596)) ;
#87506=CARTESIAN_POINT('Origin',(61.5,261.2,28.7213203435596)) ;
#87507=CARTESIAN_POINT('Origin',(61.5,261.2,30.7213203435596)) ;
#87508=CARTESIAN_POINT('',(58.8,261.2,28.7213203435596)) ;
#87509=CARTESIAN_POINT('Origin',(61.5,261.2,28.7213203435596)) ;
#87510=CARTESIAN_POINT('',(58.8,261.2,30.7213203435596)) ;
#87511=CARTESIAN_POINT('Origin',(61.5,261.2,28.7213203435596)) ;
#117133=UNCERTAINTY_MEASURE_WITH_UNIT(LENGTH_MEASURE(0.01),#117171,
'DISTANCE_ACCURACY_VALUE',
'Maximum model space distance between geometric entities at asserted c
onnectivities') ;
#117147=UNCERTAINTY_MEASURE_WITH_UNIT(LENGTH_MEASURE(0.01),#117171,
'DISTANCE_ACCURACY_VALUE',
'Maximum model space distance between geometric entities at asserted c
onnectivities') ;
#117156=(
GEOMETRIC_REPRESENTATION_CONTEXT(3)
GLOBAL_UNCERTAINTY_ASSIGNED_CONTEXT((#117133))
GLOBAL_UNIT_ASSIGNED_CONTEXT((#117171,#117173,#117174))
REPRESENTATION_CONTEXT('','3D')
) ;
#117170=(
GEOMETRIC_REPRESENTATION_CONTEXT(3)
GLOBAL_UNCERTAINTY_ASSIGNED_CONTEXT((#117147))
GLOBAL_UNIT_ASSIGNED_CONTEXT((#117171,#117173,#117174))
REPRESENTATION_CONTEXT('','3D')
) ;
#117171=(
LENGTH_UNIT()
NAMED_UNIT(*)
SI_UNIT(.MILLI.,.METRE.)
) ;
#117173=(
NAMED_UNIT(*)
PLANE_ANGLE_UNIT()
SI_UNIT($,.RADIAN.)
) ;
#117174=(
NAMED_UNIT(*)
SI_UNIT($,.STERADIAN.)
SOLID_ANGLE_UNIT()
) ;
#117183=SHAPE_DEFINITION_REPRESENTATION(#117205,#117248) ;
#117205=PRODUCT_DEFINITION_SHAPE('',$,#117271) ;
#117248=SHAPE_REPRESENTATION('',(#51993),#117156) ;
#117262=PRODUCT_DEFINITION_CONTEXT('part definition',#117330,'design') ;
#117271=PRODUCT_DEFINITION('Spring_Washer_2','Spring_Washer_2',#117293,
#117262) ;
#117293=PRODUCT_DEFINITION_FORMATION('',$,#117340) ;
#117330=APPLICATION_CONTEXT(
'Core Data for Automotive Mechanical Design Process') ;
#117331=PRODUCT_CONTEXT('part definition',#117330,'mechanical') ;
#117340=PRODUCT('Spring_Washer_2','Spring_Washer_2',$,(#117331)) ;
#117355=PRESENTATION_STYLE_ASSIGNMENT((#117357)) ;
#117357=SURFACE_STYLE_USAGE(.BOTH.,#117359) ;
#117359=SURFACE_SIDE_STYLE('',(#117361)) ;
#117361=SURFACE_STYLE_FILL_AREA(#117363) ;
#117363=FILL_AREA_STYLE('Opaque(160,160,160)',(#117365)) ;
#117365=FILL_AREA_STYLE_COLOUR('Opaque(160,160,160)',#117367) ;
#117367=COLOUR_RGB('Opaque(160,160,160)', 0.09019608, 0.27058824, 0.51372549) ;
ENDSEC;
END-ISO-10303-21;
